ISO-10303-21;
HEADER;
/* Generated by software containing ST-Developer
 * from STEP Tools, Inc. (www.steptools.com) 
 */

FILE_DESCRIPTION(
/* description */ ('STEP AP214'),
/* implementation_level */ '2;1');

FILE_NAME(
/* name */ 'Heavy Hex Bolt 0.625-18 x 2.5 x 1.25.step',
/* time_stamp */ '2026-11-14T07:13:32-08:00',
/* author */ (''),
/* organization */ (''),
/* preprocessor_version */ 'ST-DEVELOPER v20.2',
/* originating_system */ 'Autodesk Translation Framework v15.17.0.0',
/* authorisation */ '');

FILE_SCHEMA (('AUTOMOTIVE_DESIGN { 1 0 10303 214 3 1 1 }'));
ENDSEC;

DATA;
#10=MECHANICAL_DESIGN_GEOMETRIC_PRESENTATION_REPRESENTATION('',(#1320),#32903);
#420=(
BOUNDED_CURVE()
B_SPLINE_CURVE(2,(#22829,#22830,#22831),.UNSPECIFIED.,.F.,.F.)
B_SPLINE_CURVE_WITH_KNOTS((3,3),(2.04583671611078,3.43014356426221),
 .UNSPECIFIED.)
CURVE()
GEOMETRIC_REPRESENTATION_ITEM()
RATIONAL_B_SPLINE_CURVE((1.65994685877124,1.78834419513798,1.78834419513798))
REPRESENTATION_ITEM('')
);
#421=(
BOUNDED_CURVE()
B_SPLINE_CURVE(2,(#22838,#22839,#22840),.UNSPECIFIED.,.F.,.F.)
B_SPLINE_CURVE_WITH_KNOTS((3,3),(3.43014356426221,4.81445041241362),
 .UNSPECIFIED.)
CURVE()
GEOMETRIC_REPRESENTATION_ITEM()
RATIONAL_B_SPLINE_CURVE((1.78834419513797,1.78834419513797,1.65994685877124))
REPRESENTATION_ITEM('')
);
#422=(
BOUNDED_CURVE()
B_SPLINE_CURVE(2,(#22844,#22845,#22846),.UNSPECIFIED.,.F.,.F.)
B_SPLINE_CURVE_WITH_KNOTS((3,3),(2.04583671611079,3.4301435642622),
 .UNSPECIFIED.)
CURVE()
GEOMETRIC_REPRESENTATION_ITEM()
RATIONAL_B_SPLINE_CURVE((1.65994685877124,1.78834419513797,1.78834419513797))
REPRESENTATION_ITEM('')
);
#423=(
BOUNDED_CURVE()
B_SPLINE_CURVE(2,(#22850,#22851,#22852),.UNSPECIFIED.,.F.,.F.)
B_SPLINE_CURVE_WITH_KNOTS((3,3),(3.4301435642622,4.81445041241363),
 .UNSPECIFIED.)
CURVE()
GEOMETRIC_REPRESENTATION_ITEM()
RATIONAL_B_SPLINE_CURVE((1.78834419513797,1.78834419513797,1.65994685877124))
REPRESENTATION_ITEM('')
);
#424=(
BOUNDED_CURVE()
B_SPLINE_CURVE(2,(#22856,#22857,#22858),.UNSPECIFIED.,.F.,.F.)
B_SPLINE_CURVE_WITH_KNOTS((3,3),(2.04583671611079,3.43014356426221),
 .UNSPECIFIED.)
CURVE()
GEOMETRIC_REPRESENTATION_ITEM()
RATIONAL_B_SPLINE_CURVE((1.65994685877124,1.78834419513797,1.78834419513797))
REPRESENTATION_ITEM('')
);
#425=(
BOUNDED_CURVE()
B_SPLINE_CURVE(2,(#22862,#22863,#22864),.UNSPECIFIED.,.F.,.F.)
B_SPLINE_CURVE_WITH_KNOTS((3,3),(3.43014356426221,4.81445041241362),
 .UNSPECIFIED.)
CURVE()
GEOMETRIC_REPRESENTATION_ITEM()
RATIONAL_B_SPLINE_CURVE((1.78834419513797,1.78834419513797,1.65994685877124))
REPRESENTATION_ITEM('')
);
#426=(
BOUNDED_CURVE()
B_SPLINE_CURVE(2,(#22868,#22869,#22870),.UNSPECIFIED.,.F.,.F.)
B_SPLINE_CURVE_WITH_KNOTS((3,3),(2.04583671611078,3.4301435642622),
 .UNSPECIFIED.)
CURVE()
GEOMETRIC_REPRESENTATION_ITEM()
RATIONAL_B_SPLINE_CURVE((1.65994685877124,1.78834419513797,1.78834419513797))
REPRESENTATION_ITEM('')
);
#427=(
BOUNDED_CURVE()
B_SPLINE_CURVE(2,(#22874,#22875,#22876),.UNSPECIFIED.,.F.,.F.)
B_SPLINE_CURVE_WITH_KNOTS((3,3),(3.4301435642622,4.81445041241362),
 .UNSPECIFIED.)
CURVE()
GEOMETRIC_REPRESENTATION_ITEM()
RATIONAL_B_SPLINE_CURVE((1.78834419513797,1.78834419513797,1.65994685877124))
REPRESENTATION_ITEM('')
);
#428=(
BOUNDED_CURVE()
B_SPLINE_CURVE(2,(#22880,#22881,#22882),.UNSPECIFIED.,.F.,.F.)
B_SPLINE_CURVE_WITH_KNOTS((3,3),(2.04583671611079,3.4301435642622),
 .UNSPECIFIED.)
CURVE()
GEOMETRIC_REPRESENTATION_ITEM()
RATIONAL_B_SPLINE_CURVE((1.65994685877124,1.78834419513797,1.78834419513797))
REPRESENTATION_ITEM('')
);
#429=(
BOUNDED_CURVE()
B_SPLINE_CURVE(2,(#22886,#22887,#22888),.UNSPECIFIED.,.F.,.F.)
B_SPLINE_CURVE_WITH_KNOTS((3,3),(3.4301435642622,4.81445041241362),
 .UNSPECIFIED.)
CURVE()
GEOMETRIC_REPRESENTATION_ITEM()
RATIONAL_B_SPLINE_CURVE((1.78834419513797,1.78834419513797,1.65994685877124))
REPRESENTATION_ITEM('')
);
#430=(
BOUNDED_CURVE()
B_SPLINE_CURVE(2,(#22891,#22892,#22893),.UNSPECIFIED.,.F.,.F.)
B_SPLINE_CURVE_WITH_KNOTS((3,3),(2.04583671611079,3.4301435642622),
 .UNSPECIFIED.)
CURVE()
GEOMETRIC_REPRESENTATION_ITEM()
RATIONAL_B_SPLINE_CURVE((1.65994685877124,1.78834419513797,1.78834419513797))
REPRESENTATION_ITEM('')
);
#431=(
BOUNDED_CURVE()
B_SPLINE_CURVE(2,(#22895,#22896,#22897),.UNSPECIFIED.,.F.,.F.)
B_SPLINE_CURVE_WITH_KNOTS((3,3),(3.4301435642622,4.81445041241363),
 .UNSPECIFIED.)
CURVE()
GEOMETRIC_REPRESENTATION_ITEM()
RATIONAL_B_SPLINE_CURVE((1.78834419513797,1.78834419513797,1.65994685877124))
REPRESENTATION_ITEM('')
);
#581=CONICAL_SURFACE('',#16304,7.09803,0.785398163397444);
#582=CONICAL_SURFACE('',#16317,13.4874,1.0471975511966);
#583=CONICAL_SURFACE('',#16319,13.4874,1.0471975511966);
#584=CONICAL_SURFACE('',#16321,13.4874,1.0471975511966);
#585=CONICAL_SURFACE('',#16323,13.4874,1.0471975511966);
#586=CONICAL_SURFACE('',#16325,13.4874,1.0471975511966);
#587=CONICAL_SURFACE('',#16327,13.4874,1.0471975511966);
#677=SHAPE_REPRESENTATION_RELATIONSHIP('SRR','None',#33019,#691);
#691=ADVANCED_BREP_SHAPE_REPRESENTATION('',(#1409),#32894);
#891=CIRCLE('',#16305,7.9375);
#892=CIRCLE('',#16306,7.09803);
#893=CIRCLE('',#16308,7.9375);
#894=CIRCLE('',#16318,13.4874);
#895=CIRCLE('',#16320,13.4874);
#896=CIRCLE('',#16322,13.4874);
#897=CIRCLE('',#16324,13.4874);
#898=CIRCLE('',#16326,13.4874);
#899=CIRCLE('',#16328,13.4874);
#1183=CYLINDRICAL_SURFACE('',#16307,7.9375);
#1320=STYLED_ITEM('',(#33099),#1409);
#1409=MANIFOLD_SOLID_BREP('Body1',#15568);
#1596=FACE_BOUND('',#3005,.T.);
#1974=FACE_OUTER_BOUND('',#2996,.T.);
#1975=FACE_OUTER_BOUND('',#2997,.T.);
#1976=FACE_OUTER_BOUND('',#2998,.T.);
#1977=FACE_OUTER_BOUND('',#2999,.T.);
#1978=FACE_OUTER_BOUND('',#3000,.T.);
#1979=FACE_OUTER_BOUND('',#3001,.T.);
#1980=FACE_OUTER_BOUND('',#3002,.T.);
#1981=FACE_OUTER_BOUND('',#3003,.T.);
#1982=FACE_OUTER_BOUND('',#3004,.T.);
#1983=FACE_OUTER_BOUND('',#3006,.T.);
#1984=FACE_OUTER_BOUND('',#3007,.T.);
#1985=FACE_OUTER_BOUND('',#3008,.T.);
#1986=FACE_OUTER_BOUND('',#3009,.T.);
#1987=FACE_OUTER_BOUND('',#3010,.T.);
#1988=FACE_OUTER_BOUND('',#3011,.T.);
#1989=FACE_OUTER_BOUND('',#3012,.T.);
#1990=FACE_OUTER_BOUND('',#3013,.T.);
#2996=EDGE_LOOP('',(#11323,#11324,#11325,#11326));
#2997=EDGE_LOOP('',(#11327,#11328,#11329,#11330));
#2998=EDGE_LOOP('',(#11331,#11332,#11333,#11334,#11335));
#2999=EDGE_LOOP('',(#11336,#11337,#11338,#11339,#11340));
#3000=EDGE_LOOP('',(#11341,#11342,#11343,#11344,#11345));
#3001=EDGE_LOOP('',(#11346,#11347,#11348,#11349,#11350));
#3002=EDGE_LOOP('',(#11351,#11352,#11353,#11354,#11355));
#3003=EDGE_LOOP('',(#11356,#11357,#11358,#11359,#11360));
#3004=EDGE_LOOP('',(#11361,#11362,#11363,#11364,#11365,#11366));
#3005=EDGE_LOOP('',(#11367));
#3006=EDGE_LOOP('',(#11368));
#3007=EDGE_LOOP('',(#11369,#11370,#11371));
#3008=EDGE_LOOP('',(#11372,#11373,#11374));
#3009=EDGE_LOOP('',(#11375,#11376,#11377));
#3010=EDGE_LOOP('',(#11378,#11379,#11380));
#3011=EDGE_LOOP('',(#11381,#11382,#11383));
#3012=EDGE_LOOP('',(#11384,#11385,#11386));
#3013=EDGE_LOOP('',(#11387,#11388,#11389,#11390,#11391,#11392));
#4154=LINE('',#22820,#5558);
#4155=LINE('',#22825,#5559);
#4156=LINE('',#22833,#5560);
#4157=LINE('',#22835,#5561);
#4158=LINE('',#22837,#5562);
#4159=LINE('',#22848,#5563);
#4160=LINE('',#22849,#5564);
#4161=LINE('',#22860,#5565);
#4162=LINE('',#22861,#5566);
#4163=LINE('',#22872,#5567);
#4164=LINE('',#22873,#5568);
#4165=LINE('',#22884,#5569);
#4166=LINE('',#22885,#5570);
#4167=LINE('',#22894,#5571);
#5558=VECTOR('',#18684,7.09803);
#5559=VECTOR('',#18691,7.9375);
#5560=VECTOR('',#18694,1000.);
#5561=VECTOR('',#18695,1000.);
#5562=VECTOR('',#18696,1000.);
#5563=VECTOR('',#18699,1000.);
#5564=VECTOR('',#18700,1000.);
#5565=VECTOR('',#18703,1000.);
#5566=VECTOR('',#18704,1000.);
#5567=VECTOR('',#18707,1000.);
#5568=VECTOR('',#18708,1000.);
#5569=VECTOR('',#18711,1000.);
#5570=VECTOR('',#18712,1000.);
#5571=VECTOR('',#18715,1000.);
#6950=VERTEX_POINT('',#22817);
#6951=VERTEX_POINT('',#22819);
#6952=VERTEX_POINT('',#22823);
#6953=VERTEX_POINT('',#22827);
#6954=VERTEX_POINT('',#22828);
#6955=VERTEX_POINT('',#22832);
#6956=VERTEX_POINT('',#22834);
#6957=VERTEX_POINT('',#22836);
#6958=VERTEX_POINT('',#22842);
#6959=VERTEX_POINT('',#22843);
#6960=VERTEX_POINT('',#22847);
#6961=VERTEX_POINT('',#22854);
#6962=VERTEX_POINT('',#22855);
#6963=VERTEX_POINT('',#22859);
#6964=VERTEX_POINT('',#22866);
#6965=VERTEX_POINT('',#22867);
#6966=VERTEX_POINT('',#22871);
#6967=VERTEX_POINT('',#22878);
#6968=VERTEX_POINT('',#22879);
#6969=VERTEX_POINT('',#22883);
#6970=VERTEX_POINT('',#22890);
#8545=EDGE_CURVE('',#6950,#6950,#891,.T.);
#8546=EDGE_CURVE('',#6950,#6951,#4154,.T.);
#8547=EDGE_CURVE('',#6951,#6951,#892,.T.);
#8548=EDGE_CURVE('',#6952,#6952,#893,.T.);
#8549=EDGE_CURVE('',#6952,#6950,#4155,.T.);
#8550=EDGE_CURVE('',#6953,#6954,#420,.T.);
#8551=EDGE_CURVE('',#6955,#6953,#4156,.T.);
#8552=EDGE_CURVE('',#6956,#6955,#4157,.T.);
#8553=EDGE_CURVE('',#6956,#6957,#4158,.T.);
#8554=EDGE_CURVE('',#6954,#6957,#421,.T.);
#8555=EDGE_CURVE('',#6958,#6959,#422,.T.);
#8556=EDGE_CURVE('',#6960,#6958,#4159,.T.);
#8557=EDGE_CURVE('',#6955,#6960,#4160,.T.);
#8558=EDGE_CURVE('',#6959,#6953,#423,.T.);
#8559=EDGE_CURVE('',#6961,#6962,#424,.T.);
#8560=EDGE_CURVE('',#6963,#6961,#4161,.T.);
#8561=EDGE_CURVE('',#6960,#6963,#4162,.T.);
#8562=EDGE_CURVE('',#6962,#6958,#425,.T.);
#8563=EDGE_CURVE('',#6964,#6965,#426,.T.);
#8564=EDGE_CURVE('',#6966,#6964,#4163,.T.);
#8565=EDGE_CURVE('',#6963,#6966,#4164,.T.);
#8566=EDGE_CURVE('',#6965,#6961,#427,.T.);
#8567=EDGE_CURVE('',#6967,#6968,#428,.T.);
#8568=EDGE_CURVE('',#6969,#6967,#4165,.T.);
#8569=EDGE_CURVE('',#6966,#6969,#4166,.T.);
#8570=EDGE_CURVE('',#6968,#6964,#429,.T.);
#8571=EDGE_CURVE('',#6957,#6970,#430,.T.);
#8572=EDGE_CURVE('',#6969,#6956,#4167,.T.);
#8573=EDGE_CURVE('',#6970,#6967,#431,.T.);
#8574=EDGE_CURVE('',#6968,#6970,#894,.T.);
#8575=EDGE_CURVE('',#6965,#6968,#895,.T.);
#8576=EDGE_CURVE('',#6962,#6965,#896,.T.);
#8577=EDGE_CURVE('',#6962,#6959,#897,.T.);
#8578=EDGE_CURVE('',#6954,#6959,#898,.T.);
#8579=EDGE_CURVE('',#6970,#6954,#899,.T.);
#11323=ORIENTED_EDGE('',*,*,#8545,.F.);
#11324=ORIENTED_EDGE('',*,*,#8546,.T.);
#11325=ORIENTED_EDGE('',*,*,#8547,.T.);
#11326=ORIENTED_EDGE('',*,*,#8546,.F.);
#11327=ORIENTED_EDGE('',*,*,#8548,.F.);
#11328=ORIENTED_EDGE('',*,*,#8549,.T.);
#11329=ORIENTED_EDGE('',*,*,#8545,.T.);
#11330=ORIENTED_EDGE('',*,*,#8549,.F.);
#11331=ORIENTED_EDGE('',*,*,#8550,.F.);
#11332=ORIENTED_EDGE('',*,*,#8551,.F.);
#11333=ORIENTED_EDGE('',*,*,#8552,.F.);
#11334=ORIENTED_EDGE('',*,*,#8553,.T.);
#11335=ORIENTED_EDGE('',*,*,#8554,.F.);
#11336=ORIENTED_EDGE('',*,*,#8555,.F.);
#11337=ORIENTED_EDGE('',*,*,#8556,.F.);
#11338=ORIENTED_EDGE('',*,*,#8557,.F.);
#11339=ORIENTED_EDGE('',*,*,#8551,.T.);
#11340=ORIENTED_EDGE('',*,*,#8558,.F.);
#11341=ORIENTED_EDGE('',*,*,#8559,.F.);
#11342=ORIENTED_EDGE('',*,*,#8560,.F.);
#11343=ORIENTED_EDGE('',*,*,#8561,.F.);
#11344=ORIENTED_EDGE('',*,*,#8556,.T.);
#11345=ORIENTED_EDGE('',*,*,#8562,.F.);
#11346=ORIENTED_EDGE('',*,*,#8563,.F.);
#11347=ORIENTED_EDGE('',*,*,#8564,.F.);
#11348=ORIENTED_EDGE('',*,*,#8565,.F.);
#11349=ORIENTED_EDGE('',*,*,#8560,.T.);
#11350=ORIENTED_EDGE('',*,*,#8566,.F.);
#11351=ORIENTED_EDGE('',*,*,#8567,.F.);
#11352=ORIENTED_EDGE('',*,*,#8568,.F.);
#11353=ORIENTED_EDGE('',*,*,#8569,.F.);
#11354=ORIENTED_EDGE('',*,*,#8564,.T.);
#11355=ORIENTED_EDGE('',*,*,#8570,.F.);
#11356=ORIENTED_EDGE('',*,*,#8571,.F.);
#11357=ORIENTED_EDGE('',*,*,#8553,.F.);
#11358=ORIENTED_EDGE('',*,*,#8572,.F.);
#11359=ORIENTED_EDGE('',*,*,#8568,.T.);
#11360=ORIENTED_EDGE('',*,*,#8573,.F.);
#11361=ORIENTED_EDGE('',*,*,#8552,.T.);
#11362=ORIENTED_EDGE('',*,*,#8557,.T.);
#11363=ORIENTED_EDGE('',*,*,#8561,.T.);
#11364=ORIENTED_EDGE('',*,*,#8565,.T.);
#11365=ORIENTED_EDGE('',*,*,#8569,.T.);
#11366=ORIENTED_EDGE('',*,*,#8572,.T.);
#11367=ORIENTED_EDGE('',*,*,#8548,.T.);
#11368=ORIENTED_EDGE('',*,*,#8547,.F.);
#11369=ORIENTED_EDGE('',*,*,#8567,.T.);
#11370=ORIENTED_EDGE('',*,*,#8574,.T.);
#11371=ORIENTED_EDGE('',*,*,#8573,.T.);
#11372=ORIENTED_EDGE('',*,*,#8563,.T.);
#11373=ORIENTED_EDGE('',*,*,#8575,.T.);
#11374=ORIENTED_EDGE('',*,*,#8570,.T.);
#11375=ORIENTED_EDGE('',*,*,#8559,.T.);
#11376=ORIENTED_EDGE('',*,*,#8576,.T.);
#11377=ORIENTED_EDGE('',*,*,#8566,.T.);
#11378=ORIENTED_EDGE('',*,*,#8562,.T.);
#11379=ORIENTED_EDGE('',*,*,#8555,.T.);
#11380=ORIENTED_EDGE('',*,*,#8577,.F.);
#11381=ORIENTED_EDGE('',*,*,#8558,.T.);
#11382=ORIENTED_EDGE('',*,*,#8550,.T.);
#11383=ORIENTED_EDGE('',*,*,#8578,.T.);
#11384=ORIENTED_EDGE('',*,*,#8554,.T.);
#11385=ORIENTED_EDGE('',*,*,#8571,.T.);
#11386=ORIENTED_EDGE('',*,*,#8579,.T.);
#11387=ORIENTED_EDGE('',*,*,#8579,.F.);
#11388=ORIENTED_EDGE('',*,*,#8574,.F.);
#11389=ORIENTED_EDGE('',*,*,#8575,.F.);
#11390=ORIENTED_EDGE('',*,*,#8576,.F.);
#11391=ORIENTED_EDGE('',*,*,#8577,.T.);
#11392=ORIENTED_EDGE('',*,*,#8578,.F.);
#14234=PLANE('',#16309);
#14235=PLANE('',#16310);
#14236=PLANE('',#16311);
#14237=PLANE('',#16312);
#14238=PLANE('',#16313);
#14239=PLANE('',#16314);
#14240=PLANE('',#16315);
#14241=PLANE('',#16316);
#14242=PLANE('',#16329);
#14942=ADVANCED_FACE('',(#1974),#581,.T.);
#14943=ADVANCED_FACE('',(#1975),#1183,.T.);
#14944=ADVANCED_FACE('',(#1976),#14234,.F.);
#14945=ADVANCED_FACE('',(#1977),#14235,.F.);
#14946=ADVANCED_FACE('',(#1978),#14236,.F.);
#14947=ADVANCED_FACE('',(#1979),#14237,.F.);
#14948=ADVANCED_FACE('',(#1980),#14238,.F.);
#14949=ADVANCED_FACE('',(#1981),#14239,.F.);
#14950=ADVANCED_FACE('',(#1982,#1596),#14240,.T.);
#14951=ADVANCED_FACE('',(#1983),#14241,.F.);
#14952=ADVANCED_FACE('',(#1984),#582,.T.);
#14953=ADVANCED_FACE('',(#1985),#583,.T.);
#14954=ADVANCED_FACE('',(#1986),#584,.T.);
#14955=ADVANCED_FACE('',(#1987),#585,.T.);
#14956=ADVANCED_FACE('',(#1988),#586,.T.);
#14957=ADVANCED_FACE('',(#1989),#587,.T.);
#14958=ADVANCED_FACE('',(#1990),#14242,.F.);
#15568=CLOSED_SHELL('',(#14942,#14943,#14944,#14945,#14946,#14947,#14948,
#14949,#14950,#14951,#14952,#14953,#14954,#14955,#14956,#14957,#14958));
#16303=AXIS2_PLACEMENT_3D('',#22815,#18678,#18679);
#16304=AXIS2_PLACEMENT_3D('',#22816,#18680,#18681);
#16305=AXIS2_PLACEMENT_3D('',#22818,#18682,#18683);
#16306=AXIS2_PLACEMENT_3D('',#22821,#18685,#18686);
#16307=AXIS2_PLACEMENT_3D('',#22822,#18687,#18688);
#16308=AXIS2_PLACEMENT_3D('',#22824,#18689,#18690);
#16309=AXIS2_PLACEMENT_3D('',#22826,#18692,#18693);
#16310=AXIS2_PLACEMENT_3D('',#22841,#18697,#18698);
#16311=AXIS2_PLACEMENT_3D('',#22853,#18701,#18702);
#16312=AXIS2_PLACEMENT_3D('',#22865,#18705,#18706);
#16313=AXIS2_PLACEMENT_3D('',#22877,#18709,#18710);
#16314=AXIS2_PLACEMENT_3D('',#22889,#18713,#18714);
#16315=AXIS2_PLACEMENT_3D('',#22898,#18716,#18717);
#16316=AXIS2_PLACEMENT_3D('',#22899,#18718,#18719);
#16317=AXIS2_PLACEMENT_3D('',#22900,#18720,#18721);
#16318=AXIS2_PLACEMENT_3D('',#22901,#18722,#18723);
#16319=AXIS2_PLACEMENT_3D('',#22902,#18724,#18725);
#16320=AXIS2_PLACEMENT_3D('',#22903,#18726,#18727);
#16321=AXIS2_PLACEMENT_3D('',#22904,#18728,#18729);
#16322=AXIS2_PLACEMENT_3D('',#22905,#18730,#18731);
#16323=AXIS2_PLACEMENT_3D('',#22906,#18732,#18733);
#16324=AXIS2_PLACEMENT_3D('',#22907,#18734,#18735);
#16325=AXIS2_PLACEMENT_3D('',#22908,#18736,#18737);
#16326=AXIS2_PLACEMENT_3D('',#22909,#18738,#18739);
#16327=AXIS2_PLACEMENT_3D('',#22910,#18740,#18741);
#16328=AXIS2_PLACEMENT_3D('',#22911,#18742,#18743);
#16329=AXIS2_PLACEMENT_3D('',#22912,#18744,#18745);
#18678=DIRECTION('axis',(0.,0.,1.));
#18679=DIRECTION('refdir',(1.,0.,0.));
#18680=DIRECTION('center_axis',(-1.,0.,0.));
#18681=DIRECTION('ref_axis',(0.,0.,1.));
#18682=DIRECTION('center_axis',(-1.,0.,0.));
#18683=DIRECTION('ref_axis',(0.,0.,1.));
#18684=DIRECTION('',(0.707106781186551,8.65956056235489E-17,0.707106781186544));
#18685=DIRECTION('center_axis',(-1.,0.,0.));
#18686=DIRECTION('ref_axis',(0.,0.,1.));
#18687=DIRECTION('center_axis',(-1.,0.,0.));
#18688=DIRECTION('ref_axis',(0.,0.,1.));
#18689=DIRECTION('center_axis',(-1.,0.,0.));
#18690=DIRECTION('ref_axis',(0.,0.,-1.));
#18691=DIRECTION('',(1.,0.,0.));
#18692=DIRECTION('center_axis',(0.,-0.866025403784438,0.500000000000001));
#18693=DIRECTION('ref_axis',(0.,-0.500000000000001,-0.866025403784438));
#18694=DIRECTION('',(-1.,0.,0.));
#18695=DIRECTION('',(0.,0.500000000000001,0.866025403784438));
#18696=DIRECTION('',(-1.,0.,0.));
#18697=DIRECTION('center_axis',(0.,-0.866025403784438,-0.500000000000001));
#18698=DIRECTION('ref_axis',(0.,0.500000000000001,-0.866025403784438));
#18699=DIRECTION('',(-1.,0.,0.));
#18700=DIRECTION('',(0.,-0.500000000000001,0.866025403784438));
#18701=DIRECTION('center_axis',(0.,-2.22773047249605E-16,-1.));
#18702=DIRECTION('ref_axis',(0.,1.,-2.22773047249605E-16));
#18703=DIRECTION('',(-1.,0.,0.));
#18704=DIRECTION('',(0.,-1.,2.22773047249605E-16));
#18705=DIRECTION('center_axis',(0.,0.866025403784438,-0.500000000000002));
#18706=DIRECTION('ref_axis',(0.,0.500000000000002,0.866025403784438));
#18707=DIRECTION('',(-1.,0.,0.));
#18708=DIRECTION('',(0.,-0.500000000000002,-0.866025403784437));
#18709=DIRECTION('center_axis',(0.,0.866025403784439,0.5));
#18710=DIRECTION('ref_axis',(0.,-0.5,0.866025403784439));
#18711=DIRECTION('',(-1.,0.,0.));
#18712=DIRECTION('',(0.,0.5,-0.866025403784439));
#18713=DIRECTION('center_axis',(0.,-1.11386523624802E-16,1.));
#18714=DIRECTION('ref_axis',(0.,-1.,-1.11386523624802E-16));
#18715=DIRECTION('',(0.,1.,1.11386523624802E-16));
#18716=DIRECTION('center_axis',(1.,0.,0.));
#18717=DIRECTION('ref_axis',(0.,0.,-1.));
#18718=DIRECTION('center_axis',(-1.,0.,0.));
#18719=DIRECTION('ref_axis',(0.,0.,1.));
#18720=DIRECTION('center_axis',(1.,0.,0.));
#18721=DIRECTION('ref_axis',(0.,0.,-1.));
#18722=DIRECTION('center_axis',(1.,0.,0.));
#18723=DIRECTION('ref_axis',(0.,0.,-1.));
#18724=DIRECTION('center_axis',(1.,0.,0.));
#18725=DIRECTION('ref_axis',(0.,0.,-1.));
#18726=DIRECTION('center_axis',(1.,0.,0.));
#18727=DIRECTION('ref_axis',(0.,0.,-1.));
#18728=DIRECTION('center_axis',(1.,0.,0.));
#18729=DIRECTION('ref_axis',(0.,0.,-1.));
#18730=DIRECTION('center_axis',(1.,0.,0.));
#18731=DIRECTION('ref_axis',(0.,0.,-1.));
#18732=DIRECTION('center_axis',(1.,0.,0.));
#18733=DIRECTION('ref_axis',(0.,0.,-1.));
#18734=DIRECTION('center_axis',(-1.,0.,0.));
#18735=DIRECTION('ref_axis',(0.,0.,1.));
#18736=DIRECTION('center_axis',(1.,0.,0.));
#18737=DIRECTION('ref_axis',(0.,0.,-1.));
#18738=DIRECTION('center_axis',(1.,0.,0.));
#18739=DIRECTION('ref_axis',(0.,0.,-1.));
#18740=DIRECTION('center_axis',(1.,0.,0.));
#18741=DIRECTION('ref_axis',(0.,0.,-1.));
#18742=DIRECTION('center_axis',(1.,0.,0.));
#18743=DIRECTION('ref_axis',(0.,0.,-1.));
#18744=DIRECTION('center_axis',(1.,0.,0.));
#18745=DIRECTION('ref_axis',(0.,0.,-1.));
#22815=CARTESIAN_POINT('',(0.,0.,0.));
#22816=CARTESIAN_POINT('Origin',(74.7776,0.,0.));
#22817=CARTESIAN_POINT('',(73.93813,-9.72063396823212E-16,-7.93750000000001));
#22818=CARTESIAN_POINT('Origin',(73.93813,0.,0.));
#22819=CARTESIAN_POINT('',(74.7776,-8.69257971975189E-16,-7.09803));
#22820=CARTESIAN_POINT('',(74.7776,-8.69257971975189E-16,-7.09803));
#22821=CARTESIAN_POINT('Origin',(74.7776,0.,0.));
#22822=CARTESIAN_POINT('Origin',(0.,0.,0.));
#22823=CARTESIAN_POINT('',(11.2776,-9.72063396823212E-16,-7.9375));
#22824=CARTESIAN_POINT('Origin',(11.2776,0.,0.));
#22825=CARTESIAN_POINT('',(0.,-9.72063396823212E-16,-7.9375));
#22826=CARTESIAN_POINT('Origin',(11.2776,7.78695402066815,-13.4874));
#22827=CARTESIAN_POINT('',(1.20464597933184,15.5739080413363,-3.66756626076851E-16));
#22828=CARTESIAN_POINT('',(0.,11.6804310310022,-6.74370000000002));
#22829=CARTESIAN_POINT('Ctrl Pts',(1.20464597933471,15.5739080413413,8.62737789681159E-12));
#22830=CARTESIAN_POINT('Ctrl Pts',(-9.65894031423886E-15,13.487400000002,
-3.61393793799208));
#22831=CARTESIAN_POINT('Ctrl Pts',(-5.4631332398222E-15,11.6804310310022,
-6.74370000000003));
#22832=CARTESIAN_POINT('',(11.2776,15.5739080413363,0.));
#22833=CARTESIAN_POINT('',(11.2776,15.5739080413363,0.));
#22834=CARTESIAN_POINT('',(11.2776,7.78695402066815,-13.4874));
#22835=CARTESIAN_POINT('',(11.2776,7.78695402066815,-13.4874));
#22836=CARTESIAN_POINT('',(1.20464597933183,7.78695402066815,-13.4874));
#22837=CARTESIAN_POINT('',(11.2776,7.78695402066815,-13.4874));
#22838=CARTESIAN_POINT('Ctrl Pts',(-5.4631332398222E-15,11.6804310310022,
-6.74370000000003));
#22839=CARTESIAN_POINT('Ctrl Pts',(-1.64537630913334E-15,9.87346206200246,
-9.87346206200795));
#22840=CARTESIAN_POINT('Ctrl Pts',(1.2046459793347,7.78695402066317,-13.4874000000086));
#22841=CARTESIAN_POINT('Origin',(11.2776,15.5739080413363,0.));
#22842=CARTESIAN_POINT('',(1.20464597933183,7.78695402066815,13.4874));
#22843=CARTESIAN_POINT('',(0.,11.6804310310022,6.74370000000002));
#22844=CARTESIAN_POINT('Ctrl Pts',(1.2046459793347,7.78695402066316,13.4874000000086));
#22845=CARTESIAN_POINT('Ctrl Pts',(3.33066907387547E-16,9.87346206200246,
9.87346206200796));
#22846=CARTESIAN_POINT('Ctrl Pts',(4.96648476347475E-16,11.6804310310022,
6.74370000000002));
#22847=CARTESIAN_POINT('',(11.2776,7.78695402066815,13.4874));
#22848=CARTESIAN_POINT('',(11.2776,7.78695402066815,13.4874));
#22849=CARTESIAN_POINT('',(11.2776,15.5739080413363,0.));
#22850=CARTESIAN_POINT('Ctrl Pts',(4.96648476347475E-16,11.6804310310022,
6.74370000000002));
#22851=CARTESIAN_POINT('Ctrl Pts',(4.75437074788592E-16,13.487400000002,
3.61393793799208));
#22852=CARTESIAN_POINT('Ctrl Pts',(1.20464597933472,15.5739080413413,-8.6123960944604E-12));
#22853=CARTESIAN_POINT('Origin',(11.2776,7.78695402066815,13.4874));
#22854=CARTESIAN_POINT('',(1.20464597933183,-7.78695402066814,13.4874));
#22855=CARTESIAN_POINT('',(0.,3.00462919747433E-15,13.4874));
#22856=CARTESIAN_POINT('Ctrl Pts',(1.2046459793347,-7.78695402067809,13.4874));
#22857=CARTESIAN_POINT('Ctrl Pts',(-4.21884749357559E-15,-3.61393793799951,
13.4874));
#22858=CARTESIAN_POINT('Ctrl Pts',(-2.48324238173737E-15,1.39061573377293E-14,
13.4874));
#22859=CARTESIAN_POINT('',(11.2776,-7.78695402066814,13.4874));
#22860=CARTESIAN_POINT('',(11.2776,-7.78695402066814,13.4874));
#22861=CARTESIAN_POINT('',(11.2776,7.78695402066815,13.4874));
#22862=CARTESIAN_POINT('Ctrl Pts',(-2.48324238173737E-15,1.39061573377293E-14,
13.4874));
#22863=CARTESIAN_POINT('Ctrl Pts',(-1.12263434420355E-15,3.61393793799953,
13.4874));
#22864=CARTESIAN_POINT('Ctrl Pts',(1.2046459793347,7.7869540206781,13.4874));
#22865=CARTESIAN_POINT('Origin',(11.2776,-15.5739080413363,0.));
#22866=CARTESIAN_POINT('',(1.20464597933184,-15.5739080413363,3.75592506952845E-16));
#22867=CARTESIAN_POINT('',(0.,-11.6804310310022,6.74370000000003));
#22868=CARTESIAN_POINT('Ctrl Pts',(1.20464597933472,-15.5739080413413,-8.61774673815726E-12));
#22869=CARTESIAN_POINT('Ctrl Pts',(2.1094237467878E-15,-13.487400000002,
3.61393793799208));
#22870=CARTESIAN_POINT('Ctrl Pts',(4.96648476347477E-16,-11.6804310310022,
6.74370000000002));
#22871=CARTESIAN_POINT('',(11.2776,-15.5739080413363,0.));
#22872=CARTESIAN_POINT('',(11.2776,-15.5739080413363,0.));
#22873=CARTESIAN_POINT('',(11.2776,-15.5739080413363,0.));
#22874=CARTESIAN_POINT('Ctrl Pts',(4.96648476347477E-16,-11.6804310310022,
6.74370000000002));
#22875=CARTESIAN_POINT('Ctrl Pts',(-9.58335530627874E-16,-9.87346206200246,
9.87346206200795));
#22876=CARTESIAN_POINT('Ctrl Pts',(1.2046459793347,-7.78695402066317,13.4874000000086));
#22877=CARTESIAN_POINT('Origin',(11.2776,-7.78695402066817,-13.4874));
#22878=CARTESIAN_POINT('',(1.20464597933184,-7.78695402066817,-13.4874));
#22879=CARTESIAN_POINT('',(0.,-11.6804310310022,-6.7437));
#22880=CARTESIAN_POINT('Ctrl Pts',(1.20464597933471,-7.7869540206632,-13.4874000000086));
#22881=CARTESIAN_POINT('Ctrl Pts',(8.43769498715119E-15,-9.87346206200249,
-9.87346206200795));
#22882=CARTESIAN_POINT('Ctrl Pts',(8.93967257425456E-15,-11.6804310310023,
-6.74370000000001));
#22883=CARTESIAN_POINT('',(11.2776,-7.78695402066817,-13.4874));
#22884=CARTESIAN_POINT('',(11.2776,-7.78695402066817,-13.4874));
#22885=CARTESIAN_POINT('',(11.2776,-7.78695402066817,-13.4874));
#22886=CARTESIAN_POINT('Ctrl Pts',(8.93967257425456E-15,-11.6804310310023,
-6.74370000000001));
#22887=CARTESIAN_POINT('Ctrl Pts',(9.09553207322584E-15,-13.487400000002,
-3.61393793799206));
#22888=CARTESIAN_POINT('Ctrl Pts',(1.20464597933472,-15.5739080413413,8.63486879798721E-12));
#22889=CARTESIAN_POINT('Origin',(11.2776,7.78695402066815,-13.4874));
#22890=CARTESIAN_POINT('',(0.,1.50231459873716E-15,-13.4874));
#22891=CARTESIAN_POINT('Ctrl Pts',(1.2046459793347,7.7869540206781,-13.4874));
#22892=CARTESIAN_POINT('Ctrl Pts',(-2.55351295663786E-15,3.61393793799952,
-13.4874));
#22893=CARTESIAN_POINT('Ctrl Pts',(-2.23491814356364E-15,1.9865939053899E-15,
-13.4874));
#22894=CARTESIAN_POINT('',(11.2776,7.78695402066815,-13.4874));
#22895=CARTESIAN_POINT('Ctrl Pts',(-2.23491814356364E-15,1.9865939053899E-15,
-13.4874));
#22896=CARTESIAN_POINT('Ctrl Pts',(-2.22907762438719E-15,-3.61393793799953,
-13.4874));
#22897=CARTESIAN_POINT('Ctrl Pts',(1.20464597933471,-7.78695402067813,-13.4874));
#22898=CARTESIAN_POINT('Origin',(11.2776,15.5739080413363,-1.3010426069826E-15));
#22899=CARTESIAN_POINT('Origin',(74.7776,0.,0.));
#22900=CARTESIAN_POINT('Origin',(0.,0.,0.));
#22901=CARTESIAN_POINT('Origin',(0.,0.,0.));
#22902=CARTESIAN_POINT('Origin',(0.,0.,0.));
#22903=CARTESIAN_POINT('Origin',(0.,0.,0.));
#22904=CARTESIAN_POINT('Origin',(0.,0.,0.));
#22905=CARTESIAN_POINT('Origin',(0.,0.,0.));
#22906=CARTESIAN_POINT('Origin',(0.,0.,0.));
#22907=CARTESIAN_POINT('Origin',(0.,0.,0.));
#22908=CARTESIAN_POINT('Origin',(0.,0.,0.));
#22909=CARTESIAN_POINT('Origin',(0.,0.,0.));
#22910=CARTESIAN_POINT('Origin',(0.,0.,0.));
#22911=CARTESIAN_POINT('Origin',(0.,0.,0.));
#22912=CARTESIAN_POINT('Origin',(0.,15.5739080413363,-1.3010426069826E-15));
#32877=UNCERTAINTY_MEASURE_WITH_UNIT(LENGTH_MEASURE(0.01),#32904,
'DISTANCE_ACCURACY_VALUE',
'Maximum model space distance between geometric entities at asserted c
onnectivities');
#32886=UNCERTAINTY_MEASURE_WITH_UNIT(LENGTH_MEASURE(0.01),#32904,
'DISTANCE_ACCURACY_VALUE',
'Maximum model space distance between geometric entities at asserted c
onnectivities');
#32894=(
GEOMETRIC_REPRESENTATION_CONTEXT(3)
GLOBAL_UNCERTAINTY_ASSIGNED_CONTEXT((#32877))
GLOBAL_UNIT_ASSIGNED_CONTEXT((#32904,#32906,#32907))
REPRESENTATION_CONTEXT('','3D')
);
#32903=(
GEOMETRIC_REPRESENTATION_CONTEXT(3)
GLOBAL_UNCERTAINTY_ASSIGNED_CONTEXT((#32886))
GLOBAL_UNIT_ASSIGNED_CONTEXT((#32904,#32906,#32907))
REPRESENTATION_CONTEXT('','3D')
);
#32904=(
LENGTH_UNIT()
NAMED_UNIT(*)
SI_UNIT(.MILLI.,.METRE.)
);
#32906=(
NAMED_UNIT(*)
PLANE_ANGLE_UNIT()
SI_UNIT($,.RADIAN.)
);
#32907=(
NAMED_UNIT(*)
SI_UNIT($,.STERADIAN.)
SOLID_ANGLE_UNIT()
);
#32915=SHAPE_DEFINITION_REPRESENTATION(#32931,#33019);
#32931=PRODUCT_DEFINITION_SHAPE('',$,#33036);
#33019=SHAPE_REPRESENTATION('',(#16303),#32894);
#33028=PRODUCT_DEFINITION_CONTEXT('part definition',#33078,'design');
#33036=PRODUCT_DEFINITION('Heavy Hex Bolt 0.625-18 x 2.5 x 1.25',
'Heavy Hex Bolt 0.625-18 x 2.5 x 1.25',#33052,#33028);
#33052=PRODUCT_DEFINITION_FORMATION('',$,#33087);
#33078=APPLICATION_CONTEXT(
'Core Data for Automotive Mechanical Design Process');
#33079=PRODUCT_CONTEXT('part definition',#33078,'mechanical');
#33087=PRODUCT('Heavy Hex Bolt 0.625-18 x 2.5 x 1.25',
'Heavy Hex Bolt 0.625-18 x 2.5 x 1.25',$,(#33079));
#33099=PRESENTATION_STYLE_ASSIGNMENT((#33105));
#33105=SURFACE_STYLE_USAGE(.BOTH.,#33111);
#33111=SURFACE_SIDE_STYLE('',(#33117));
#33117=SURFACE_STYLE_FILL_AREA(#33123);
#33123=FILL_AREA_STYLE('Opaque(31,36,43)',(#33129));
#33129=FILL_AREA_STYLE_COLOUR('Opaque(31,36,43)',#33135);
#33135=COLOUR_RGB('Opaque(31,36,43)',0.12156862745098,0.141176470588235,
0.168627450980392);
ENDSEC;
END-ISO-10303-21;
